ISO-10303-21;
HEADER;
/* Generated by software containing ST-Developer
 * from STEP Tools, Inc. (www.steptools.com) 
 */

FILE_DESCRIPTION(
/* description */ ('Four-bar tabletop demonstrator'),
/* implementation_level */ '2;1');

FILE_NAME(
/* name */ 'M4x10 Cap Screw.step',
/* time_stamp */ '2026-10-29T17:05:23-07:00',
/* author */ (''),
/* organization */ (''),
/* preprocessor_version */ 'ST-DEVELOPER v20.2',
/* originating_system */ 'Autodesk Translation Framework v15.17.0.0',
/* authorisation */ '');

FILE_SCHEMA (('AUTOMOTIVE_DESIGN { 1 0 10303 214 3 1 1 }'));
ENDSEC;

DATA;
#10=MECHANICAL_DESIGN_GEOMETRIC_PRESENTATION_REPRESENTATION('',(#355),#6705);
#272=CONICAL_SURFACE('',#3935,0.325,0.785398163397448);
#273=CONICAL_SURFACE('',#3939,0.335,0.785398163397448);
#274=CONICAL_SURFACE('',#3943,0.21,0.463647609000806);
#277=ORIENTED_CLOSED_SHELL('',*,#3400,.F.);
#279=BREP_WITH_VOIDS('Body1',#3401,(#277));
#317=SHAPE_REPRESENTATION_RELATIONSHIP('SRR','None',#6826,#332);
#332=ADVANCED_BREP_SHAPE_REPRESENTATION('',(#279),#6699);
#355=STYLED_ITEM('',(#6996),#279);
#450=FACE_BOUND('',#999,.T.);
#528=PLANE('',#3923);
#529=PLANE('',#3924);
#530=PLANE('',#3925);
#531=PLANE('',#3926);
#532=PLANE('',#3927);
#533=PLANE('',#3928);
#534=PLANE('',#3929);
#535=PLANE('',#3930);
#536=PLANE('',#3931);
#537=PLANE('',#3933);
#538=PLANE('',#3941);
#713=FACE_OUTER_BOUND('',#985,.T.);
#714=FACE_OUTER_BOUND('',#986,.T.);
#715=FACE_OUTER_BOUND('',#987,.T.);
#716=FACE_OUTER_BOUND('',#988,.T.);
#717=FACE_OUTER_BOUND('',#989,.T.);
#718=FACE_OUTER_BOUND('',#990,.T.);
#719=FACE_OUTER_BOUND('',#991,.T.);
#720=FACE_OUTER_BOUND('',#992,.T.);
#721=FACE_OUTER_BOUND('',#993,.T.);
#722=FACE_OUTER_BOUND('',#994,.T.);
#723=FACE_OUTER_BOUND('',#995,.T.);
#724=FACE_OUTER_BOUND('',#996,.T.);
#725=FACE_OUTER_BOUND('',#997,.T.);
#726=FACE_OUTER_BOUND('',#998,.T.);
#727=FACE_OUTER_BOUND('',#1000,.T.);
#728=FACE_OUTER_BOUND('',#1001,.T.);
#985=EDGE_LOOP('',(#2906,#2907,#2908,#2909));
#986=EDGE_LOOP('',(#2910,#2911,#2912,#2913));
#987=EDGE_LOOP('',(#2914,#2915,#2916,#2917));
#988=EDGE_LOOP('',(#2918,#2919,#2920,#2921));
#989=EDGE_LOOP('',(#2922,#2923,#2924,#2925));
#990=EDGE_LOOP('',(#2926,#2927,#2928,#2929));
#991=EDGE_LOOP('',(#2930,#2931,#2932,#2933,#2934,#2935));
#992=EDGE_LOOP('',(#2936,#2937,#2938,#2939,#2940,#2941));
#993=EDGE_LOOP('',(#2942));
#994=EDGE_LOOP('',(#2943));
#995=EDGE_LOOP('',(#2944,#2945,#2946,#2947));
#996=EDGE_LOOP('',(#2948,#2949,#2950,#2951));
#997=EDGE_LOOP('',(#2952,#2953,#2954,#2955));
#998=EDGE_LOOP('',(#2956));
#999=EDGE_LOOP('',(#2957));
#1000=EDGE_LOOP('',(#2958,#2959,#2960,#2961));
#1001=EDGE_LOOP('',(#2962,#2963,#2964,#2965));
#1157=LINE('',#6329,#1327);
#1158=LINE('',#6331,#1328);
#1159=LINE('',#6333,#1329);
#1160=LINE('',#6334,#1330);
#1161=LINE('',#6337,#1331);
#1162=LINE('',#6339,#1332);
#1163=LINE('',#6340,#1333);
#1164=LINE('',#6343,#1334);
#1165=LINE('',#6345,#1335);
#1166=LINE('',#6346,#1336);
#1167=LINE('',#6349,#1337);
#1168=LINE('',#6351,#1338);
#1169=LINE('',#6352,#1339);
#1170=LINE('',#6355,#1340);
#1171=LINE('',#6357,#1341);
#1172=LINE('',#6358,#1342);
#1173=LINE('',#6360,#1343);
#1174=LINE('',#6361,#1344);
#1175=LINE('',#6373,#1345);
#1176=LINE('',#6377,#1346);
#1177=LINE('',#6381,#1347);
#1178=LINE('',#6388,#1348);
#1179=LINE('',#6390,#1349);
#1327=VECTOR('',#4878,1.);
#1328=VECTOR('',#4879,1.);
#1329=VECTOR('',#4880,1.);
#1330=VECTOR('',#4881,1.);
#1331=VECTOR('',#4884,1.);
#1332=VECTOR('',#4885,1.);
#1333=VECTOR('',#4886,1.);
#1334=VECTOR('',#4889,1.);
#1335=VECTOR('',#4890,1.);
#1336=VECTOR('',#4891,1.);
#1337=VECTOR('',#4894,1.);
#1338=VECTOR('',#4895,1.);
#1339=VECTOR('',#4896,1.);
#1340=VECTOR('',#4899,1.);
#1341=VECTOR('',#4900,1.);
#1342=VECTOR('',#4901,1.);
#1343=VECTOR('',#4904,1.);
#1344=VECTOR('',#4905,1.);
#1345=VECTOR('',#4922,0.325);
#1346=VECTOR('',#4927,0.35);
#1347=VECTOR('',#4932,0.335);
#1348=VECTOR('',#4941,0.21);
#1349=VECTOR('',#4944,0.2);
#1568=CIRCLE('',#3932,0.1954);
#1569=CIRCLE('',#3934,0.3);
#1570=CIRCLE('',#3936,0.35);
#1571=CIRCLE('',#3938,0.35);
#1572=CIRCLE('',#3940,0.32);
#1573=CIRCLE('',#3942,0.22);
#1574=CIRCLE('',#3944,0.1954);
#1815=VERTEX_POINT('',#6327);
#1816=VERTEX_POINT('',#6328);
#1817=VERTEX_POINT('',#6330);
#1818=VERTEX_POINT('',#6332);
#1819=VERTEX_POINT('',#6336);
#1820=VERTEX_POINT('',#6338);
#1821=VERTEX_POINT('',#6342);
#1822=VERTEX_POINT('',#6344);
#1823=VERTEX_POINT('',#6348);
#1824=VERTEX_POINT('',#6350);
#1825=VERTEX_POINT('',#6354);
#1826=VERTEX_POINT('',#6356);
#1827=VERTEX_POINT('',#6365);
#1828=VERTEX_POINT('',#6368);
#1829=VERTEX_POINT('',#6371);
#1830=VERTEX_POINT('',#6375);
#1831=VERTEX_POINT('',#6379);
#1832=VERTEX_POINT('',#6383);
#1833=VERTEX_POINT('',#6386);
#2189=EDGE_CURVE('',#1815,#1816,#1157,.T.);
#2190=EDGE_CURVE('',#1816,#1817,#1158,.T.);
#2191=EDGE_CURVE('',#1817,#1818,#1159,.T.);
#2192=EDGE_CURVE('',#1815,#1818,#1160,.T.);
#2193=EDGE_CURVE('',#1816,#1819,#1161,.T.);
#2194=EDGE_CURVE('',#1819,#1820,#1162,.T.);
#2195=EDGE_CURVE('',#1820,#1817,#1163,.T.);
#2196=EDGE_CURVE('',#1819,#1821,#1164,.T.);
#2197=EDGE_CURVE('',#1821,#1822,#1165,.T.);
#2198=EDGE_CURVE('',#1822,#1820,#1166,.T.);
#2199=EDGE_CURVE('',#1821,#1823,#1167,.T.);
#2200=EDGE_CURVE('',#1823,#1824,#1168,.T.);
#2201=EDGE_CURVE('',#1824,#1822,#1169,.T.);
#2202=EDGE_CURVE('',#1823,#1825,#1170,.T.);
#2203=EDGE_CURVE('',#1825,#1826,#1171,.T.);
#2204=EDGE_CURVE('',#1826,#1824,#1172,.T.);
#2205=EDGE_CURVE('',#1825,#1815,#1173,.T.);
#2206=EDGE_CURVE('',#1818,#1826,#1174,.T.);
#2207=EDGE_CURVE('',#1827,#1827,#1568,.T.);
#2208=EDGE_CURVE('',#1828,#1828,#1569,.T.);
#2209=EDGE_CURVE('',#1829,#1829,#1570,.T.);
#2210=EDGE_CURVE('',#1829,#1828,#1175,.T.);
#2211=EDGE_CURVE('',#1830,#1830,#1571,.T.);
#2212=EDGE_CURVE('',#1830,#1829,#1176,.T.);
#2213=EDGE_CURVE('',#1831,#1831,#1572,.T.);
#2214=EDGE_CURVE('',#1831,#1830,#1177,.T.);
#2215=EDGE_CURVE('',#1832,#1832,#1573,.T.);
#2216=EDGE_CURVE('',#1833,#1833,#1574,.F.);
#2217=EDGE_CURVE('',#1833,#1832,#1178,.T.);
#2218=EDGE_CURVE('',#1827,#1833,#1179,.T.);
#2906=ORIENTED_EDGE('',*,*,#2189,.T.);
#2907=ORIENTED_EDGE('',*,*,#2190,.T.);
#2908=ORIENTED_EDGE('',*,*,#2191,.T.);
#2909=ORIENTED_EDGE('',*,*,#2192,.F.);
#2910=ORIENTED_EDGE('',*,*,#2193,.T.);
#2911=ORIENTED_EDGE('',*,*,#2194,.T.);
#2912=ORIENTED_EDGE('',*,*,#2195,.T.);
#2913=ORIENTED_EDGE('',*,*,#2190,.F.);
#2914=ORIENTED_EDGE('',*,*,#2196,.T.);
#2915=ORIENTED_EDGE('',*,*,#2197,.T.);
#2916=ORIENTED_EDGE('',*,*,#2198,.T.);
#2917=ORIENTED_EDGE('',*,*,#2194,.F.);
#2918=ORIENTED_EDGE('',*,*,#2199,.T.);
#2919=ORIENTED_EDGE('',*,*,#2200,.T.);
#2920=ORIENTED_EDGE('',*,*,#2201,.T.);
#2921=ORIENTED_EDGE('',*,*,#2197,.F.);
#2922=ORIENTED_EDGE('',*,*,#2202,.T.);
#2923=ORIENTED_EDGE('',*,*,#2203,.T.);
#2924=ORIENTED_EDGE('',*,*,#2204,.T.);
#2925=ORIENTED_EDGE('',*,*,#2200,.F.);
#2926=ORIENTED_EDGE('',*,*,#2205,.T.);
#2927=ORIENTED_EDGE('',*,*,#2192,.T.);
#2928=ORIENTED_EDGE('',*,*,#2206,.T.);
#2929=ORIENTED_EDGE('',*,*,#2203,.F.);
#2930=ORIENTED_EDGE('',*,*,#2205,.F.);
#2931=ORIENTED_EDGE('',*,*,#2202,.F.);
#2932=ORIENTED_EDGE('',*,*,#2199,.F.);
#2933=ORIENTED_EDGE('',*,*,#2196,.F.);
#2934=ORIENTED_EDGE('',*,*,#2193,.F.);
#2935=ORIENTED_EDGE('',*,*,#2189,.F.);
#2936=ORIENTED_EDGE('',*,*,#2206,.F.);
#2937=ORIENTED_EDGE('',*,*,#2191,.F.);
#2938=ORIENTED_EDGE('',*,*,#2195,.F.);
#2939=ORIENTED_EDGE('',*,*,#2198,.F.);
#2940=ORIENTED_EDGE('',*,*,#2201,.F.);
#2941=ORIENTED_EDGE('',*,*,#2204,.F.);
#2942=ORIENTED_EDGE('',*,*,#2207,.F.);
#2943=ORIENTED_EDGE('',*,*,#2208,.F.);
#2944=ORIENTED_EDGE('',*,*,#2209,.F.);
#2945=ORIENTED_EDGE('',*,*,#2210,.T.);
#2946=ORIENTED_EDGE('',*,*,#2208,.T.);
#2947=ORIENTED_EDGE('',*,*,#2210,.F.);
#2948=ORIENTED_EDGE('',*,*,#2211,.F.);
#2949=ORIENTED_EDGE('',*,*,#2212,.T.);
#2950=ORIENTED_EDGE('',*,*,#2209,.T.);
#2951=ORIENTED_EDGE('',*,*,#2212,.F.);
#2952=ORIENTED_EDGE('',*,*,#2213,.F.);
#2953=ORIENTED_EDGE('',*,*,#2214,.T.);
#2954=ORIENTED_EDGE('',*,*,#2211,.T.);
#2955=ORIENTED_EDGE('',*,*,#2214,.F.);
#2956=ORIENTED_EDGE('',*,*,#2213,.T.);
#2957=ORIENTED_EDGE('',*,*,#2215,.F.);
#2958=ORIENTED_EDGE('',*,*,#2216,.F.);
#2959=ORIENTED_EDGE('',*,*,#2217,.T.);
#2960=ORIENTED_EDGE('',*,*,#2215,.T.);
#2961=ORIENTED_EDGE('',*,*,#2217,.F.);
#2962=ORIENTED_EDGE('',*,*,#2207,.T.);
#2963=ORIENTED_EDGE('',*,*,#2218,.T.);
#2964=ORIENTED_EDGE('',*,*,#2216,.T.);
#2965=ORIENTED_EDGE('',*,*,#2218,.F.);
#3164=CYLINDRICAL_SURFACE('',#3937,0.35);
#3165=CYLINDRICAL_SURFACE('',#3945,0.1954);
#3329=ADVANCED_FACE('',(#713),#528,.F.);
#3330=ADVANCED_FACE('',(#714),#529,.F.);
#3331=ADVANCED_FACE('',(#715),#530,.F.);
#3332=ADVANCED_FACE('',(#716),#531,.F.);
#3333=ADVANCED_FACE('',(#717),#532,.F.);
#3334=ADVANCED_FACE('',(#718),#533,.F.);
#3335=ADVANCED_FACE('',(#719),#534,.F.);
#3336=ADVANCED_FACE('',(#720),#535,.F.);
#3337=ADVANCED_FACE('',(#721),#536,.F.);
#3338=ADVANCED_FACE('',(#722),#537,.T.);
#3339=ADVANCED_FACE('',(#723),#272,.T.);
#3340=ADVANCED_FACE('',(#724),#3164,.T.);
#3341=ADVANCED_FACE('',(#725),#273,.T.);
#3342=ADVANCED_FACE('',(#726,#450),#538,.T.);
#3343=ADVANCED_FACE('',(#727),#274,.T.);
#3344=ADVANCED_FACE('',(#728),#3165,.T.);
#3400=CLOSED_SHELL('',(#3329,#3330,#3331,#3332,#3333,#3334,#3335,#3336));
#3401=CLOSED_SHELL('',(#3337,#3338,#3339,#3340,#3341,#3342,#3343,#3344));
#3922=AXIS2_PLACEMENT_3D('',#6325,#4874,#4875);
#3923=AXIS2_PLACEMENT_3D('',#6326,#4876,#4877);
#3924=AXIS2_PLACEMENT_3D('',#6335,#4882,#4883);
#3925=AXIS2_PLACEMENT_3D('',#6341,#4887,#4888);
#3926=AXIS2_PLACEMENT_3D('',#6347,#4892,#4893);
#3927=AXIS2_PLACEMENT_3D('',#6353,#4897,#4898);
#3928=AXIS2_PLACEMENT_3D('',#6359,#4902,#4903);
#3929=AXIS2_PLACEMENT_3D('',#6362,#4906,#4907);
#3930=AXIS2_PLACEMENT_3D('',#6363,#4908,#4909);
#3931=AXIS2_PLACEMENT_3D('',#6364,#4910,#4911);
#3932=AXIS2_PLACEMENT_3D('',#6366,#4912,#4913);
#3933=AXIS2_PLACEMENT_3D('',#6367,#4914,#4915);
#3934=AXIS2_PLACEMENT_3D('',#6369,#4916,#4917);
#3935=AXIS2_PLACEMENT_3D('',#6370,#4918,#4919);
#3936=AXIS2_PLACEMENT_3D('',#6372,#4920,#4921);
#3937=AXIS2_PLACEMENT_3D('',#6374,#4923,#4924);
#3938=AXIS2_PLACEMENT_3D('',#6376,#4925,#4926);
#3939=AXIS2_PLACEMENT_3D('',#6378,#4928,#4929);
#3940=AXIS2_PLACEMENT_3D('',#6380,#4930,#4931);
#3941=AXIS2_PLACEMENT_3D('',#6382,#4933,#4934);
#3942=AXIS2_PLACEMENT_3D('',#6384,#4935,#4936);
#3943=AXIS2_PLACEMENT_3D('',#6385,#4937,#4938);
#3944=AXIS2_PLACEMENT_3D('',#6387,#4939,#4940);
#3945=AXIS2_PLACEMENT_3D('',#6389,#4942,#4943);
#4874=DIRECTION('axis',(0.,0.,1.));
#4875=DIRECTION('refdir',(1.,0.,0.));
#4876=DIRECTION('center_axis',(0.866025403784439,0.,-0.5));
#4877=DIRECTION('ref_axis',(0.5,0.,0.866025403784439));
#4878=DIRECTION('',(-0.5,0.,-0.866025403784439));
#4879=DIRECTION('',(0.,-1.,0.));
#4880=DIRECTION('',(0.5,0.,0.866025403784439));
#4881=DIRECTION('',(0.,-1.,0.));
#4882=DIRECTION('center_axis',(1.60246890531964E-16,0.,-1.));
#4883=DIRECTION('ref_axis',(1.,0.,1.60246890531964E-16));
#4884=DIRECTION('',(-1.,0.,-1.60246890531964E-16));
#4885=DIRECTION('',(0.,-1.,0.));
#4886=DIRECTION('',(1.,0.,1.60246890531964E-16));
#4887=DIRECTION('center_axis',(-0.866025403784439,0.,-0.5));
#4888=DIRECTION('ref_axis',(0.5,0.,-0.866025403784439));
#4889=DIRECTION('',(-0.5,0.,0.866025403784439));
#4890=DIRECTION('',(0.,-1.,0.));
#4891=DIRECTION('',(0.5,0.,-0.866025403784439));
#4892=DIRECTION('center_axis',(-0.866025403784439,0.,0.5));
#4893=DIRECTION('ref_axis',(-0.5,0.,-0.866025403784439));
#4894=DIRECTION('',(0.5,0.,0.866025403784439));
#4895=DIRECTION('',(0.,-1.,0.));
#4896=DIRECTION('',(-0.5,0.,-0.866025403784439));
#4897=DIRECTION('center_axis',(-1.60246890531964E-16,0.,1.));
#4898=DIRECTION('ref_axis',(-1.,0.,-1.60246890531964E-16));
#4899=DIRECTION('',(1.,0.,1.60246890531964E-16));
#4900=DIRECTION('',(0.,-1.,0.));
#4901=DIRECTION('',(-1.,0.,-1.60246890531964E-16));
#4902=DIRECTION('center_axis',(0.866025403784439,0.,0.5));
#4903=DIRECTION('ref_axis',(-0.5,0.,0.866025403784439));
#4904=DIRECTION('',(0.5,0.,-0.866025403784439));
#4905=DIRECTION('',(-0.5,0.,0.866025403784439));
#4906=DIRECTION('center_axis',(0.,1.,0.));
#4907=DIRECTION('ref_axis',(1.,0.,0.));
#4908=DIRECTION('center_axis',(0.,-1.,0.));
#4909=DIRECTION('ref_axis',(0.,0.,-1.));
#4910=DIRECTION('center_axis',(0.,1.,0.));
#4911=DIRECTION('ref_axis',(1.,0.,0.));
#4912=DIRECTION('center_axis',(0.,1.,0.));
#4913=DIRECTION('ref_axis',(1.,0.,0.));
#4914=DIRECTION('center_axis',(0.,1.,0.));
#4915=DIRECTION('ref_axis',(0.,0.,1.));
#4916=DIRECTION('center_axis',(0.,-1.,0.));
#4917=DIRECTION('ref_axis',(1.,0.,0.));
#4918=DIRECTION('center_axis',(0.,-1.,0.));
#4919=DIRECTION('ref_axis',(1.,0.,0.));
#4920=DIRECTION('center_axis',(0.,-1.,0.));
#4921=DIRECTION('ref_axis',(1.,0.,0.));
#4922=DIRECTION('',(0.707106781186547,0.707106781186548,8.65956056235493E-17));
#4923=DIRECTION('center_axis',(0.,-1.,0.));
#4924=DIRECTION('ref_axis',(1.,0.,0.));
#4925=DIRECTION('center_axis',(0.,-1.,0.));
#4926=DIRECTION('ref_axis',(1.,0.,0.));
#4927=DIRECTION('',(0.,1.,0.));
#4928=DIRECTION('center_axis',(0.,1.,0.));
#4929=DIRECTION('ref_axis',(1.,0.,0.));
#4930=DIRECTION('center_axis',(0.,-1.,0.));
#4931=DIRECTION('ref_axis',(1.,0.,0.));
#4932=DIRECTION('',(-0.707106781186547,0.707106781186548,-8.65956056235493E-17));
#4933=DIRECTION('center_axis',(0.,-1.,0.));
#4934=DIRECTION('ref_axis',(0.,0.,-1.));
#4935=DIRECTION('center_axis',(0.,-1.,0.));
#4936=DIRECTION('ref_axis',(1.,0.,0.));
#4937=DIRECTION('center_axis',(0.,1.,0.));
#4938=DIRECTION('ref_axis',(1.,0.,0.));
#4939=DIRECTION('center_axis',(0.,1.,0.));
#4940=DIRECTION('ref_axis',(1.,0.,0.));
#4941=DIRECTION('',(-0.447213595499958,0.894427190999916,-5.47678698264203E-17));
#4942=DIRECTION('center_axis',(0.,-1.,0.));
#4943=DIRECTION('ref_axis',(1.,0.,0.));
#4944=DIRECTION('',(0.,1.,0.));
#6325=CARTESIAN_POINT('',(0.,0.,0.));
#6326=CARTESIAN_POINT('Origin',(0.0866025403784439,-0.4,-0.15));
#6327=CARTESIAN_POINT('',(0.173205080756888,-0.4,0.));
#6328=CARTESIAN_POINT('',(0.0866025403784439,-0.4,-0.15));
#6329=CARTESIAN_POINT('',(0.173205080756888,-0.4,0.));
#6330=CARTESIAN_POINT('',(0.0866025403784439,-0.64,-0.15));
#6331=CARTESIAN_POINT('',(0.0866025403784439,-0.4,-0.15));
#6332=CARTESIAN_POINT('',(0.173205080756888,-0.64,0.));
#6333=CARTESIAN_POINT('',(0.173205080756888,-0.64,0.));
#6334=CARTESIAN_POINT('',(0.173205080756888,-0.4,0.));
#6335=CARTESIAN_POINT('Origin',(-0.0866025403784438,-0.4,-0.15));
#6336=CARTESIAN_POINT('',(-0.0866025403784438,-0.4,-0.15));
#6337=CARTESIAN_POINT('',(0.0866025403784439,-0.4,-0.15));
#6338=CARTESIAN_POINT('',(-0.0866025403784438,-0.64,-0.15));
#6339=CARTESIAN_POINT('',(-0.0866025403784438,-0.4,-0.15));
#6340=CARTESIAN_POINT('',(0.0866025403784439,-0.64,-0.15));
#6341=CARTESIAN_POINT('Origin',(-0.173205080756888,-0.4,-2.77555756156289E-17));
#6342=CARTESIAN_POINT('',(-0.173205080756888,-0.4,-2.12115047744981E-17));
#6343=CARTESIAN_POINT('',(-0.0866025403784438,-0.4,-0.15));
#6344=CARTESIAN_POINT('',(-0.173205080756888,-0.64,-2.77555756156289E-17));
#6345=CARTESIAN_POINT('',(-0.173205080756888,-0.4,-2.12115047744981E-17));
#6346=CARTESIAN_POINT('',(-0.0866025403784438,-0.64,-0.15));
#6347=CARTESIAN_POINT('Origin',(-0.0866025403784439,-0.4,0.15));
#6348=CARTESIAN_POINT('',(-0.0866025403784439,-0.4,0.15));
#6349=CARTESIAN_POINT('',(-0.173205080756888,-0.4,-2.12115047744981E-17));
#6350=CARTESIAN_POINT('',(-0.0866025403784439,-0.64,0.15));
#6351=CARTESIAN_POINT('',(-0.0866025403784439,-0.4,0.15));
#6352=CARTESIAN_POINT('',(-0.173205080756888,-0.64,-2.12115047744981E-17));
#6353=CARTESIAN_POINT('Origin',(0.0866025403784439,-0.4,0.15));
#6354=CARTESIAN_POINT('',(0.0866025403784439,-0.4,0.15));
#6355=CARTESIAN_POINT('',(-0.0866025403784439,-0.4,0.15));
#6356=CARTESIAN_POINT('',(0.0866025403784439,-0.64,0.15));
#6357=CARTESIAN_POINT('',(0.0866025403784439,-0.4,0.15));
#6358=CARTESIAN_POINT('',(-0.0866025403784439,-0.64,0.15));
#6359=CARTESIAN_POINT('Origin',(0.173205080756888,-0.4,0.));
#6360=CARTESIAN_POINT('',(0.0866025403784439,-0.4,0.15));
#6361=CARTESIAN_POINT('',(0.0866025403784439,-0.64,0.15));
#6362=CARTESIAN_POINT('Origin',(0.,-0.4,-2.77555756156289E-17));
#6363=CARTESIAN_POINT('Origin',(0.,-0.64,-2.77555756156289E-17));
#6364=CARTESIAN_POINT('Origin',(0.,-1.,0.));
#6365=CARTESIAN_POINT('',(-0.1954,-1.,2.39295984553393E-17));
#6366=CARTESIAN_POINT('Origin',(0.,-1.,0.));
#6367=CARTESIAN_POINT('Origin',(0.3,0.4,0.));
#6368=CARTESIAN_POINT('',(-0.3,0.4,-3.67394039744206E-17));
#6369=CARTESIAN_POINT('Origin',(0.,0.4,0.));
#6370=CARTESIAN_POINT('Origin',(0.,0.375,0.));
#6371=CARTESIAN_POINT('',(-0.35,0.35,-4.28626379701573E-17));
#6372=CARTESIAN_POINT('Origin',(0.,0.35,0.));
#6373=CARTESIAN_POINT('',(-0.325,0.375,-3.9801020972289E-17));
#6374=CARTESIAN_POINT('Origin',(0.,0.19,0.));
#6375=CARTESIAN_POINT('',(-0.35,0.03,-4.28626379701574E-17));
#6376=CARTESIAN_POINT('Origin',(0.,0.03,0.));
#6377=CARTESIAN_POINT('',(-0.35,0.19,-4.28626379701574E-17));
#6378=CARTESIAN_POINT('Origin',(0.,0.0149999999999999,0.));
#6379=CARTESIAN_POINT('',(-0.32,-3.29597460435593E-17,-3.91886975727153E-17));
#6380=CARTESIAN_POINT('Origin',(0.,0.,0.));
#6381=CARTESIAN_POINT('',(-0.335,0.0149999999999999,-4.10256677714363E-17));
#6382=CARTESIAN_POINT('Origin',(0.22,0.,0.));
#6383=CARTESIAN_POINT('',(-0.22,-6.93889390390723E-18,-2.69422295812418E-17));
#6384=CARTESIAN_POINT('Origin',(0.,0.,0.));
#6385=CARTESIAN_POINT('Origin',(0.,-0.02,0.));
#6386=CARTESIAN_POINT('',(-0.1954,-0.0492,2.39295984553393E-17));
#6387=CARTESIAN_POINT('Origin',(0.,-0.0492,0.));
#6388=CARTESIAN_POINT('',(-0.21,-0.02,-2.57175827820944E-17));
#6389=CARTESIAN_POINT('Origin',(0.,-0.8,0.));
#6390=CARTESIAN_POINT('',(-0.1954,-0.8,-2.39295984553393E-17));
#6677=UNCERTAINTY_MEASURE_WITH_UNIT(LENGTH_MEASURE(0.001),#6706,
'DISTANCE_ACCURACY_VALUE',
'Maximum model space distance between geometric entities at asserted c
onnectivities');
#6683=UNCERTAINTY_MEASURE_WITH_UNIT(LENGTH_MEASURE(0.001),#6706,
'DISTANCE_ACCURACY_VALUE',
'Maximum model space distance between geometric entities at asserted c
onnectivities');
#6699=(
GEOMETRIC_REPRESENTATION_CONTEXT(3)
GLOBAL_UNCERTAINTY_ASSIGNED_CONTEXT((#6677))
GLOBAL_UNIT_ASSIGNED_CONTEXT((#6706,#6708,#6709))
REPRESENTATION_CONTEXT('','3D')
);
#6705=(
GEOMETRIC_REPRESENTATION_CONTEXT(3)
GLOBAL_UNCERTAINTY_ASSIGNED_CONTEXT((#6683))
GLOBAL_UNIT_ASSIGNED_CONTEXT((#6706,#6708,#6709))
REPRESENTATION_CONTEXT('','3D')
);
#6706=(
LENGTH_UNIT()
NAMED_UNIT(*)
SI_UNIT(.CENTI.,.METRE.)
);
#6708=(
NAMED_UNIT(*)
PLANE_ANGLE_UNIT()
SI_UNIT($,.RADIAN.)
);
#6709=(
NAMED_UNIT(*)
SI_UNIT($,.STERADIAN.)
SOLID_ANGLE_UNIT()
);
#6725=SHAPE_DEFINITION_REPRESENTATION(#6751,#6826);
#6751=PRODUCT_DEFINITION_SHAPE('',$,#6848);
#6826=SHAPE_REPRESENTATION('',(#3922),#6699);
#6832=PRODUCT_DEFINITION_CONTEXT('part definition',#6897,'design');
#6848=PRODUCT_DEFINITION('M4x10 Cap Screw','M4x10 Cap Screw',#6869,#6832);
#6869=PRODUCT_DEFINITION_FORMATION('',$,#6914);
#6897=APPLICATION_CONTEXT(
'Core Data for Automotive Mechanical Design Process');
#6898=PRODUCT_CONTEXT('part definition',#6897,'mechanical');
#6914=PRODUCT('M4x10 Cap Screw','M4x10 Cap Screw','M4x10 Cap Screw',(#6898));
#6990=COLOUR_RGB('Black',0.12,0.14,0.17);
#6991=FILL_AREA_STYLE_COLOUR('',#6990);
#6992=FILL_AREA_STYLE('',(#6991));
#6993=SURFACE_STYLE_FILL_AREA(#6992);
#6994=SURFACE_SIDE_STYLE('',(#6993));
#6995=SURFACE_STYLE_USAGE(.BOTH.,#6994);
#6996=PRESENTATION_STYLE_ASSIGNMENT((#6995));
ENDSEC;
END-ISO-10303-21;
